ISO-10303-21;
HEADER;
/* Generated by software containing ST-Developer
 * from STEP Tools, Inc. (www.steptools.com) 
 */

FILE_DESCRIPTION(
/* description */ ('XY cross-slide table'),
/* implementation_level */ '2;1');

FILE_NAME(
/* name */ 'M5x30 frame screw (1).step',
/* time_stamp */ '2026-10-28T03:22:46-07:00',
/* author */ (''),
/* organization */ (''),
/* preprocessor_version */ 'ST-DEVELOPER v20.2',
/* originating_system */ 'Autodesk Translation Framework v15.17.0.0',
/* authorisation */ '');

FILE_SCHEMA (('AUTOMOTIVE_DESIGN { 1 0 10303 214 3 1 1 }'));
ENDSEC;

DATA;
#10=MECHANICAL_DESIGN_GEOMETRIC_PRESENTATION_REPRESENTATION('',(#1769),#62984);
#24=ORIENTED_CLOSED_SHELL('',*,#23068,.F.);
#33=BREP_WITH_VOIDS('Body1',#23069,(#24));
#1479=CONICAL_SURFACE('',#25998,0.4,0.785398163397448);
#1480=CONICAL_SURFACE('',#26002,0.41,0.785398163397448);
#1481=CONICAL_SURFACE('',#26006,0.26,0.463647609000806);
#1573=SHAPE_REPRESENTATION_RELATIONSHIP('SRR','None',#63432,#1656);
#1656=ADVANCED_BREP_SHAPE_REPRESENTATION('',(#33),#62969);
#1769=STYLED_ITEM('',(#63919),#33);
#2259=FACE_BOUND('',#5577,.T.);
#2260=FACE_BOUND('',#5585,.T.);
#2771=PLANE('',#25982);
#2772=PLANE('',#25983);
#2773=PLANE('',#25984);
#2774=PLANE('',#25985);
#2775=PLANE('',#25986);
#2776=PLANE('',#25987);
#2777=PLANE('',#25988);
#2778=PLANE('',#25989);
#2779=PLANE('',#25990);
#2780=PLANE('',#25995);
#2781=PLANE('',#25996);
#2782=PLANE('',#26004);
#3882=FACE_OUTER_BOUND('',#5568,.T.);
#3883=FACE_OUTER_BOUND('',#5569,.T.);
#3884=FACE_OUTER_BOUND('',#5570,.T.);
#3885=FACE_OUTER_BOUND('',#5571,.T.);
#3886=FACE_OUTER_BOUND('',#5572,.T.);
#3887=FACE_OUTER_BOUND('',#5573,.T.);
#3888=FACE_OUTER_BOUND('',#5574,.T.);
#3889=FACE_OUTER_BOUND('',#5575,.T.);
#3890=FACE_OUTER_BOUND('',#5576,.T.);
#3891=FACE_OUTER_BOUND('',#5578,.T.);
#3892=FACE_OUTER_BOUND('',#5579,.T.);
#3893=FACE_OUTER_BOUND('',#5580,.T.);
#3894=FACE_OUTER_BOUND('',#5581,.T.);
#3895=FACE_OUTER_BOUND('',#5582,.T.);
#3896=FACE_OUTER_BOUND('',#5583,.T.);
#3897=FACE_OUTER_BOUND('',#5584,.T.);
#3898=FACE_OUTER_BOUND('',#5586,.T.);
#3899=FACE_OUTER_BOUND('',#5587,.T.);
#5568=EDGE_LOOP('',(#19546,#19547,#19548,#19549));
#5569=EDGE_LOOP('',(#19550,#19551,#19552,#19553));
#5570=EDGE_LOOP('',(#19554,#19555,#19556,#19557));
#5571=EDGE_LOOP('',(#19558,#19559,#19560,#19561));
#5572=EDGE_LOOP('',(#19562,#19563,#19564,#19565));
#5573=EDGE_LOOP('',(#19566,#19567,#19568,#19569));
#5574=EDGE_LOOP('',(#19570,#19571,#19572,#19573,#19574,#19575));
#5575=EDGE_LOOP('',(#19576,#19577,#19578,#19579,#19580,#19581));
#5576=EDGE_LOOP('',(#19582));
#5577=EDGE_LOOP('',(#19583));
#5578=EDGE_LOOP('',(#19584,#19585,#19586,#19587));
#5579=EDGE_LOOP('',(#19588));
#5580=EDGE_LOOP('',(#19589));
#5581=EDGE_LOOP('',(#19590,#19591,#19592,#19593));
#5582=EDGE_LOOP('',(#19594,#19595,#19596,#19597));
#5583=EDGE_LOOP('',(#19598,#19599,#19600,#19601));
#5584=EDGE_LOOP('',(#19602));
#5585=EDGE_LOOP('',(#19603));
#5586=EDGE_LOOP('',(#19604,#19605,#19606,#19607));
#5587=EDGE_LOOP('',(#19608,#19609,#19610,#19611));
#7055=LINE('',#50191,#8542);
#7056=LINE('',#50193,#8543);
#7057=LINE('',#50195,#8544);
#7058=LINE('',#50196,#8545);
#7059=LINE('',#50199,#8546);
#7060=LINE('',#50201,#8547);
#7061=LINE('',#50202,#8548);
#7062=LINE('',#50205,#8549);
#7063=LINE('',#50207,#8550);
#7064=LINE('',#50208,#8551);
#7065=LINE('',#50211,#8552);
#7066=LINE('',#50213,#8553);
#7067=LINE('',#50214,#8554);
#7068=LINE('',#50217,#8555);
#7069=LINE('',#50219,#8556);
#7070=LINE('',#50220,#8557);
#7071=LINE('',#50222,#8558);
#7072=LINE('',#50223,#8559);
#7073=LINE('',#50233,#8560);
#7074=LINE('',#50242,#8561);
#7075=LINE('',#50246,#8562);
#7076=LINE('',#50250,#8563);
#7077=LINE('',#50257,#8564);
#7078=LINE('',#50259,#8565);
#8542=VECTOR('',#31576,1.);
#8543=VECTOR('',#31577,1.);
#8544=VECTOR('',#31578,1.);
#8545=VECTOR('',#31579,1.);
#8546=VECTOR('',#31582,1.);
#8547=VECTOR('',#31583,1.);
#8548=VECTOR('',#31584,1.);
#8549=VECTOR('',#31587,1.);
#8550=VECTOR('',#31588,1.);
#8551=VECTOR('',#31589,1.);
#8552=VECTOR('',#31592,1.);
#8553=VECTOR('',#31593,1.);
#8554=VECTOR('',#31594,1.);
#8555=VECTOR('',#31597,1.);
#8556=VECTOR('',#31598,1.);
#8557=VECTOR('',#31599,1.);
#8558=VECTOR('',#31602,1.);
#8559=VECTOR('',#31603,1.);
#8560=VECTOR('',#31616,0.25);
#8561=VECTOR('',#31629,0.4);
#8562=VECTOR('',#31634,0.425);
#8563=VECTOR('',#31639,0.41);
#8564=VECTOR('',#31648,0.26);
#8565=VECTOR('',#31651,0.25);
#9676=CIRCLE('',#25991,0.25);
#9677=CIRCLE('',#25992,0.24505);
#9678=CIRCLE('',#25994,0.25);
#9679=CIRCLE('',#25997,0.375);
#9680=CIRCLE('',#25999,0.425);
#9681=CIRCLE('',#26001,0.425);
#9682=CIRCLE('',#26003,0.395);
#9683=CIRCLE('',#26005,0.27);
#9684=CIRCLE('',#26007,0.24505);
#11343=VERTEX_POINT('',#50189);
#11344=VERTEX_POINT('',#50190);
#11345=VERTEX_POINT('',#50192);
#11346=VERTEX_POINT('',#50194);
#11347=VERTEX_POINT('',#50198);
#11348=VERTEX_POINT('',#50200);
#11349=VERTEX_POINT('',#50204);
#11350=VERTEX_POINT('',#50206);
#11351=VERTEX_POINT('',#50210);
#11352=VERTEX_POINT('',#50212);
#11353=VERTEX_POINT('',#50216);
#11354=VERTEX_POINT('',#50218);
#11355=VERTEX_POINT('',#50227);
#11356=VERTEX_POINT('',#50229);
#11357=VERTEX_POINT('',#50232);
#11358=VERTEX_POINT('',#50237);
#11359=VERTEX_POINT('',#50240);
#11360=VERTEX_POINT('',#50244);
#11361=VERTEX_POINT('',#50248);
#11362=VERTEX_POINT('',#50252);
#11363=VERTEX_POINT('',#50255);
#14157=EDGE_CURVE('',#11343,#11344,#7055,.T.);
#14158=EDGE_CURVE('',#11344,#11345,#7056,.T.);
#14159=EDGE_CURVE('',#11345,#11346,#7057,.T.);
#14160=EDGE_CURVE('',#11343,#11346,#7058,.T.);
#14161=EDGE_CURVE('',#11344,#11347,#7059,.T.);
#14162=EDGE_CURVE('',#11347,#11348,#7060,.T.);
#14163=EDGE_CURVE('',#11348,#11345,#7061,.T.);
#14164=EDGE_CURVE('',#11347,#11349,#7062,.T.);
#14165=EDGE_CURVE('',#11349,#11350,#7063,.T.);
#14166=EDGE_CURVE('',#11350,#11348,#7064,.T.);
#14167=EDGE_CURVE('',#11349,#11351,#7065,.T.);
#14168=EDGE_CURVE('',#11351,#11352,#7066,.T.);
#14169=EDGE_CURVE('',#11352,#11350,#7067,.T.);
#14170=EDGE_CURVE('',#11351,#11353,#7068,.T.);
#14171=EDGE_CURVE('',#11353,#11354,#7069,.T.);
#14172=EDGE_CURVE('',#11354,#11352,#7070,.T.);
#14173=EDGE_CURVE('',#11353,#11343,#7071,.T.);
#14174=EDGE_CURVE('',#11346,#11354,#7072,.T.);
#14175=EDGE_CURVE('',#11355,#11355,#9676,.T.);
#14176=EDGE_CURVE('',#11356,#11356,#9677,.T.);
#14177=EDGE_CURVE('',#11355,#11357,#7073,.T.);
#14178=EDGE_CURVE('',#11357,#11357,#9678,.T.);
#14179=EDGE_CURVE('',#11358,#11358,#9679,.T.);
#14180=EDGE_CURVE('',#11359,#11359,#9680,.T.);
#14181=EDGE_CURVE('',#11359,#11358,#7074,.T.);
#14182=EDGE_CURVE('',#11360,#11360,#9681,.T.);
#14183=EDGE_CURVE('',#11360,#11359,#7075,.T.);
#14184=EDGE_CURVE('',#11361,#11361,#9682,.T.);
#14185=EDGE_CURVE('',#11361,#11360,#7076,.T.);
#14186=EDGE_CURVE('',#11362,#11362,#9683,.T.);
#14187=EDGE_CURVE('',#11363,#11363,#9684,.F.);
#14188=EDGE_CURVE('',#11363,#11362,#7077,.T.);
#14189=EDGE_CURVE('',#11356,#11363,#7078,.T.);
#19546=ORIENTED_EDGE('',*,*,#14157,.T.);
#19547=ORIENTED_EDGE('',*,*,#14158,.T.);
#19548=ORIENTED_EDGE('',*,*,#14159,.T.);
#19549=ORIENTED_EDGE('',*,*,#14160,.F.);
#19550=ORIENTED_EDGE('',*,*,#14161,.T.);
#19551=ORIENTED_EDGE('',*,*,#14162,.T.);
#19552=ORIENTED_EDGE('',*,*,#14163,.T.);
#19553=ORIENTED_EDGE('',*,*,#14158,.F.);
#19554=ORIENTED_EDGE('',*,*,#14164,.T.);
#19555=ORIENTED_EDGE('',*,*,#14165,.T.);
#19556=ORIENTED_EDGE('',*,*,#14166,.T.);
#19557=ORIENTED_EDGE('',*,*,#14162,.F.);
#19558=ORIENTED_EDGE('',*,*,#14167,.T.);
#19559=ORIENTED_EDGE('',*,*,#14168,.T.);
#19560=ORIENTED_EDGE('',*,*,#14169,.T.);
#19561=ORIENTED_EDGE('',*,*,#14165,.F.);
#19562=ORIENTED_EDGE('',*,*,#14170,.T.);
#19563=ORIENTED_EDGE('',*,*,#14171,.T.);
#19564=ORIENTED_EDGE('',*,*,#14172,.T.);
#19565=ORIENTED_EDGE('',*,*,#14168,.F.);
#19566=ORIENTED_EDGE('',*,*,#14173,.T.);
#19567=ORIENTED_EDGE('',*,*,#14160,.T.);
#19568=ORIENTED_EDGE('',*,*,#14174,.T.);
#19569=ORIENTED_EDGE('',*,*,#14171,.F.);
#19570=ORIENTED_EDGE('',*,*,#14173,.F.);
#19571=ORIENTED_EDGE('',*,*,#14170,.F.);
#19572=ORIENTED_EDGE('',*,*,#14167,.F.);
#19573=ORIENTED_EDGE('',*,*,#14164,.F.);
#19574=ORIENTED_EDGE('',*,*,#14161,.F.);
#19575=ORIENTED_EDGE('',*,*,#14157,.F.);
#19576=ORIENTED_EDGE('',*,*,#14174,.F.);
#19577=ORIENTED_EDGE('',*,*,#14159,.F.);
#19578=ORIENTED_EDGE('',*,*,#14163,.F.);
#19579=ORIENTED_EDGE('',*,*,#14166,.F.);
#19580=ORIENTED_EDGE('',*,*,#14169,.F.);
#19581=ORIENTED_EDGE('',*,*,#14172,.F.);
#19582=ORIENTED_EDGE('',*,*,#14175,.T.);
#19583=ORIENTED_EDGE('',*,*,#14176,.F.);
#19584=ORIENTED_EDGE('',*,*,#14175,.F.);
#19585=ORIENTED_EDGE('',*,*,#14177,.T.);
#19586=ORIENTED_EDGE('',*,*,#14178,.T.);
#19587=ORIENTED_EDGE('',*,*,#14177,.F.);
#19588=ORIENTED_EDGE('',*,*,#14178,.F.);
#19589=ORIENTED_EDGE('',*,*,#14179,.F.);
#19590=ORIENTED_EDGE('',*,*,#14180,.F.);
#19591=ORIENTED_EDGE('',*,*,#14181,.T.);
#19592=ORIENTED_EDGE('',*,*,#14179,.T.);
#19593=ORIENTED_EDGE('',*,*,#14181,.F.);
#19594=ORIENTED_EDGE('',*,*,#14182,.F.);
#19595=ORIENTED_EDGE('',*,*,#14183,.T.);
#19596=ORIENTED_EDGE('',*,*,#14180,.T.);
#19597=ORIENTED_EDGE('',*,*,#14183,.F.);
#19598=ORIENTED_EDGE('',*,*,#14184,.F.);
#19599=ORIENTED_EDGE('',*,*,#14185,.T.);
#19600=ORIENTED_EDGE('',*,*,#14182,.T.);
#19601=ORIENTED_EDGE('',*,*,#14185,.F.);
#19602=ORIENTED_EDGE('',*,*,#14184,.T.);
#19603=ORIENTED_EDGE('',*,*,#14186,.F.);
#19604=ORIENTED_EDGE('',*,*,#14187,.F.);
#19605=ORIENTED_EDGE('',*,*,#14188,.T.);
#19606=ORIENTED_EDGE('',*,*,#14186,.T.);
#19607=ORIENTED_EDGE('',*,*,#14188,.F.);
#19608=ORIENTED_EDGE('',*,*,#14176,.T.);
#19609=ORIENTED_EDGE('',*,*,#14189,.T.);
#19610=ORIENTED_EDGE('',*,*,#14187,.T.);
#19611=ORIENTED_EDGE('',*,*,#14189,.F.);
#21468=CYLINDRICAL_SURFACE('',#25993,0.25);
#21469=CYLINDRICAL_SURFACE('',#26000,0.425);
#21470=CYLINDRICAL_SURFACE('',#26008,0.24505);
#22663=ADVANCED_FACE('',(#3882),#2771,.F.);
#22664=ADVANCED_FACE('',(#3883),#2772,.F.);
#22665=ADVANCED_FACE('',(#3884),#2773,.F.);
#22666=ADVANCED_FACE('',(#3885),#2774,.F.);
#22667=ADVANCED_FACE('',(#3886),#2775,.F.);
#22668=ADVANCED_FACE('',(#3887),#2776,.F.);
#22669=ADVANCED_FACE('',(#3888),#2777,.F.);
#22670=ADVANCED_FACE('',(#3889),#2778,.F.);
#22671=ADVANCED_FACE('',(#3890,#2259),#2779,.T.);
#22672=ADVANCED_FACE('',(#3891),#21468,.T.);
#22673=ADVANCED_FACE('',(#3892),#2780,.F.);
#22674=ADVANCED_FACE('',(#3893),#2781,.T.);
#22675=ADVANCED_FACE('',(#3894),#1479,.T.);
#22676=ADVANCED_FACE('',(#3895),#21469,.T.);
#22677=ADVANCED_FACE('',(#3896),#1480,.T.);
#22678=ADVANCED_FACE('',(#3897,#2260),#2782,.T.);
#22679=ADVANCED_FACE('',(#3898),#1481,.T.);
#22680=ADVANCED_FACE('',(#3899),#21470,.T.);
#23068=CLOSED_SHELL('',(#22663,#22664,#22665,#22666,#22667,#22668,#22669,
#22670));
#23069=CLOSED_SHELL('',(#22671,#22672,#22673,#22674,#22675,#22676,#22677,
#22678,#22679,#22680));
#25981=AXIS2_PLACEMENT_3D('',#50187,#31572,#31573);
#25982=AXIS2_PLACEMENT_3D('',#50188,#31574,#31575);
#25983=AXIS2_PLACEMENT_3D('',#50197,#31580,#31581);
#25984=AXIS2_PLACEMENT_3D('',#50203,#31585,#31586);
#25985=AXIS2_PLACEMENT_3D('',#50209,#31590,#31591);
#25986=AXIS2_PLACEMENT_3D('',#50215,#31595,#31596);
#25987=AXIS2_PLACEMENT_3D('',#50221,#31600,#31601);
#25988=AXIS2_PLACEMENT_3D('',#50224,#31604,#31605);
#25989=AXIS2_PLACEMENT_3D('',#50225,#31606,#31607);
#25990=AXIS2_PLACEMENT_3D('',#50226,#31608,#31609);
#25991=AXIS2_PLACEMENT_3D('',#50228,#31610,#31611);
#25992=AXIS2_PLACEMENT_3D('',#50230,#31612,#31613);
#25993=AXIS2_PLACEMENT_3D('',#50231,#31614,#31615);
#25994=AXIS2_PLACEMENT_3D('',#50234,#31617,#31618);
#25995=AXIS2_PLACEMENT_3D('',#50235,#31619,#31620);
#25996=AXIS2_PLACEMENT_3D('',#50236,#31621,#31622);
#25997=AXIS2_PLACEMENT_3D('',#50238,#31623,#31624);
#25998=AXIS2_PLACEMENT_3D('',#50239,#31625,#31626);
#25999=AXIS2_PLACEMENT_3D('',#50241,#31627,#31628);
#26000=AXIS2_PLACEMENT_3D('',#50243,#31630,#31631);
#26001=AXIS2_PLACEMENT_3D('',#50245,#31632,#31633);
#26002=AXIS2_PLACEMENT_3D('',#50247,#31635,#31636);
#26003=AXIS2_PLACEMENT_3D('',#50249,#31637,#31638);
#26004=AXIS2_PLACEMENT_3D('',#50251,#31640,#31641);
#26005=AXIS2_PLACEMENT_3D('',#50253,#31642,#31643);
#26006=AXIS2_PLACEMENT_3D('',#50254,#31644,#31645);
#26007=AXIS2_PLACEMENT_3D('',#50256,#31646,#31647);
#26008=AXIS2_PLACEMENT_3D('',#50258,#31649,#31650);
#31572=DIRECTION('axis',(0.,0.,1.));
#31573=DIRECTION('refdir',(1.,0.,0.));
#31574=DIRECTION('center_axis',(0.866025403784439,0.,-0.5));
#31575=DIRECTION('ref_axis',(0.5,0.,0.866025403784439));
#31576=DIRECTION('',(-0.5,0.,-0.866025403784439));
#31577=DIRECTION('',(0.,-1.,0.));
#31578=DIRECTION('',(0.5,0.,0.866025403784439));
#31579=DIRECTION('',(0.,-1.,0.));
#31580=DIRECTION('center_axis',(1.20185167898973E-16,0.,-1.));
#31581=DIRECTION('ref_axis',(1.,0.,1.20185167898973E-16));
#31582=DIRECTION('',(-1.,0.,-1.20185167898973E-16));
#31583=DIRECTION('',(0.,-1.,0.));
#31584=DIRECTION('',(1.,0.,1.20185167898973E-16));
#31585=DIRECTION('center_axis',(-0.866025403784439,0.,-0.5));
#31586=DIRECTION('ref_axis',(0.5,0.,-0.866025403784439));
#31587=DIRECTION('',(-0.5,0.,0.866025403784439));
#31588=DIRECTION('',(0.,-1.,0.));
#31589=DIRECTION('',(0.5,0.,-0.866025403784439));
#31590=DIRECTION('center_axis',(-0.866025403784439,0.,0.5));
#31591=DIRECTION('ref_axis',(-0.5,0.,-0.866025403784439));
#31592=DIRECTION('',(0.5,0.,0.866025403784439));
#31593=DIRECTION('',(0.,-1.,0.));
#31594=DIRECTION('',(-0.5,0.,-0.866025403784439));
#31595=DIRECTION('center_axis',(-2.40370335797945E-16,0.,1.));
#31596=DIRECTION('ref_axis',(-1.,0.,-2.40370335797945E-16));
#31597=DIRECTION('',(1.,0.,2.40370335797945E-16));
#31598=DIRECTION('',(0.,-1.,0.));
#31599=DIRECTION('',(-1.,0.,-2.40370335797945E-16));
#31600=DIRECTION('center_axis',(0.866025403784439,0.,0.5));
#31601=DIRECTION('ref_axis',(-0.5,0.,0.866025403784439));
#31602=DIRECTION('',(0.5,0.,-0.866025403784439));
#31603=DIRECTION('',(-0.5,0.,0.866025403784439));
#31604=DIRECTION('center_axis',(0.,1.,0.));
#31605=DIRECTION('ref_axis',(1.,0.,0.));
#31606=DIRECTION('center_axis',(0.,-1.,0.));
#31607=DIRECTION('ref_axis',(0.,0.,-1.));
#31608=DIRECTION('center_axis',(0.,1.,0.));
#31609=DIRECTION('ref_axis',(1.,0.,0.));
#31610=DIRECTION('center_axis',(0.,1.,0.));
#31611=DIRECTION('ref_axis',(1.,0.,0.));
#31612=DIRECTION('center_axis',(0.,1.,0.));
#31613=DIRECTION('ref_axis',(1.,0.,0.));
#31614=DIRECTION('center_axis',(0.,1.,0.));
#31615=DIRECTION('ref_axis',(1.,0.,0.));
#31616=DIRECTION('',(0.,-1.,0.));
#31617=DIRECTION('center_axis',(0.,1.,0.));
#31618=DIRECTION('ref_axis',(1.,0.,0.));
#31619=DIRECTION('center_axis',(0.,1.,0.));
#31620=DIRECTION('ref_axis',(1.,0.,0.));
#31621=DIRECTION('center_axis',(0.,1.,0.));
#31622=DIRECTION('ref_axis',(0.,0.,1.));
#31623=DIRECTION('center_axis',(0.,-1.,0.));
#31624=DIRECTION('ref_axis',(1.,0.,0.));
#31625=DIRECTION('center_axis',(0.,-1.,0.));
#31626=DIRECTION('ref_axis',(1.,0.,0.));
#31627=DIRECTION('center_axis',(0.,-1.,0.));
#31628=DIRECTION('ref_axis',(1.,0.,0.));
#31629=DIRECTION('',(0.707106781186548,0.707106781186547,8.65956056235493E-17));
#31630=DIRECTION('center_axis',(0.,-1.,0.));
#31631=DIRECTION('ref_axis',(1.,0.,0.));
#31632=DIRECTION('center_axis',(0.,-1.,0.));
#31633=DIRECTION('ref_axis',(1.,0.,0.));
#31634=DIRECTION('',(0.,1.,0.));
#31635=DIRECTION('center_axis',(0.,1.,0.));
#31636=DIRECTION('ref_axis',(1.,0.,0.));
#31637=DIRECTION('center_axis',(0.,-1.,0.));
#31638=DIRECTION('ref_axis',(1.,0.,0.));
#31639=DIRECTION('',(-0.707106781186547,0.707106781186548,-8.65956056235493E-17));
#31640=DIRECTION('center_axis',(0.,-1.,0.));
#31641=DIRECTION('ref_axis',(0.,0.,-1.));
#31642=DIRECTION('center_axis',(0.,-1.,0.));
#31643=DIRECTION('ref_axis',(1.,0.,0.));
#31644=DIRECTION('center_axis',(0.,1.,0.));
#31645=DIRECTION('ref_axis',(1.,0.,0.));
#31646=DIRECTION('center_axis',(0.,1.,0.));
#31647=DIRECTION('ref_axis',(1.,0.,0.));
#31648=DIRECTION('',(-0.447213595499958,0.894427190999916,-5.47678698264203E-17));
#31649=DIRECTION('center_axis',(0.,-1.,0.));
#31650=DIRECTION('ref_axis',(1.,0.,0.));
#31651=DIRECTION('',(0.,1.,0.));
#50187=CARTESIAN_POINT('',(0.,0.,0.));
#50188=CARTESIAN_POINT('Origin',(0.115470053837925,-0.5,-0.2));
#50189=CARTESIAN_POINT('',(0.23094010767585,-0.5,0.));
#50190=CARTESIAN_POINT('',(0.115470053837925,-0.5,-0.2));
#50191=CARTESIAN_POINT('',(0.23094010767585,-0.5,0.));
#50192=CARTESIAN_POINT('',(0.115470053837925,-0.8,-0.2));
#50193=CARTESIAN_POINT('',(0.115470053837925,-0.5,-0.2));
#50194=CARTESIAN_POINT('',(0.23094010767585,-0.8,0.));
#50195=CARTESIAN_POINT('',(0.23094010767585,-0.8,0.));
#50196=CARTESIAN_POINT('',(0.23094010767585,-0.5,0.));
#50197=CARTESIAN_POINT('Origin',(-0.115470053837925,-0.5,-0.2));
#50198=CARTESIAN_POINT('',(-0.115470053837925,-0.5,-0.2));
#50199=CARTESIAN_POINT('',(0.115470053837925,-0.5,-0.2));
#50200=CARTESIAN_POINT('',(-0.115470053837925,-0.8,-0.2));
#50201=CARTESIAN_POINT('',(-0.115470053837925,-0.5,-0.2));
#50202=CARTESIAN_POINT('',(0.115470053837925,-0.8,-0.2));
#50203=CARTESIAN_POINT('Origin',(-0.23094010767585,-0.5,-2.77555756156289E-17));
#50204=CARTESIAN_POINT('',(-0.23094010767585,-0.5,-2.82820063659975E-17));
#50205=CARTESIAN_POINT('',(-0.115470053837925,-0.5,-0.2));
#50206=CARTESIAN_POINT('',(-0.23094010767585,-0.8,-2.77555756156289E-17));
#50207=CARTESIAN_POINT('',(-0.23094010767585,-0.5,-2.82820063659975E-17));
#50208=CARTESIAN_POINT('',(-0.115470053837925,-0.8,-0.2));
#50209=CARTESIAN_POINT('Origin',(-0.115470053837925,-0.5,0.2));
#50210=CARTESIAN_POINT('',(-0.115470053837925,-0.5,0.2));
#50211=CARTESIAN_POINT('',(-0.23094010767585,-0.5,-2.82820063659975E-17));
#50212=CARTESIAN_POINT('',(-0.115470053837925,-0.8,0.2));
#50213=CARTESIAN_POINT('',(-0.115470053837925,-0.5,0.2));
#50214=CARTESIAN_POINT('',(-0.23094010767585,-0.8,-2.82820063659975E-17));
#50215=CARTESIAN_POINT('Origin',(0.115470053837925,-0.5,0.2));
#50216=CARTESIAN_POINT('',(0.115470053837925,-0.5,0.2));
#50217=CARTESIAN_POINT('',(-0.115470053837925,-0.5,0.2));
#50218=CARTESIAN_POINT('',(0.115470053837925,-0.8,0.2));
#50219=CARTESIAN_POINT('',(0.115470053837925,-0.5,0.2));
#50220=CARTESIAN_POINT('',(-0.115470053837925,-0.8,0.2));
#50221=CARTESIAN_POINT('Origin',(0.23094010767585,-0.5,0.));
#50222=CARTESIAN_POINT('',(0.115470053837925,-0.5,0.2));
#50223=CARTESIAN_POINT('',(0.115470053837925,-0.8,0.2));
#50224=CARTESIAN_POINT('Origin',(0.,-0.5,0.));
#50225=CARTESIAN_POINT('Origin',(0.,-0.8,0.));
#50226=CARTESIAN_POINT('Origin',(0.,-1.9,0.));
#50227=CARTESIAN_POINT('',(-0.25,-1.9,3.06161699786838E-17));
#50228=CARTESIAN_POINT('Origin',(0.,-1.9,0.));
#50229=CARTESIAN_POINT('',(-0.24505,-1.9,3.00099698131059E-17));
#50230=CARTESIAN_POINT('Origin',(0.,-1.9,0.));
#50231=CARTESIAN_POINT('Origin',(0.,-3.,0.));
#50232=CARTESIAN_POINT('',(-0.25,-3.,3.06161699786838E-17));
#50233=CARTESIAN_POINT('',(-0.25,-3.,3.06161699786838E-17));
#50234=CARTESIAN_POINT('Origin',(0.,-3.,0.));
#50235=CARTESIAN_POINT('Origin',(0.,-3.,0.));
#50236=CARTESIAN_POINT('Origin',(0.375,0.5,0.));
#50237=CARTESIAN_POINT('',(-0.375,0.5,-4.59242549680257E-17));
#50238=CARTESIAN_POINT('Origin',(0.,0.5,0.));
#50239=CARTESIAN_POINT('Origin',(0.,0.475,0.));
#50240=CARTESIAN_POINT('',(-0.425,0.45,-5.20474889637625E-17));
#50241=CARTESIAN_POINT('Origin',(0.,0.45,0.));
#50242=CARTESIAN_POINT('',(-0.4,0.475,-4.89858719658941E-17));
#50243=CARTESIAN_POINT('Origin',(0.,0.24,0.));
#50244=CARTESIAN_POINT('',(-0.425,0.0299999999999998,-5.20474889637625E-17));
#50245=CARTESIAN_POINT('Origin',(0.,0.0299999999999998,0.));
#50246=CARTESIAN_POINT('',(-0.425,0.24,-5.20474889637625E-17));
#50247=CARTESIAN_POINT('Origin',(0.,0.0150000000000001,0.));
#50248=CARTESIAN_POINT('',(-0.395,4.85722573273506E-17,-4.83735485663204E-17));
#50249=CARTESIAN_POINT('Origin',(0.,0.,0.));
#50250=CARTESIAN_POINT('',(-0.41,0.0150000000000001,-5.02105187650415E-17));
#50251=CARTESIAN_POINT('Origin',(0.27,0.,0.));
#50252=CARTESIAN_POINT('',(-0.27,0.,-3.30654635769785E-17));
#50253=CARTESIAN_POINT('Origin',(0.,0.,0.));
#50254=CARTESIAN_POINT('Origin',(0.,-0.02,0.));
#50255=CARTESIAN_POINT('',(-0.24505,-0.0498999999999999,3.00099698131059E-17));
#50256=CARTESIAN_POINT('Origin',(0.,-0.0498999999999999,0.));
#50257=CARTESIAN_POINT('',(-0.26,-0.02,-3.18408167778312E-17));
#50258=CARTESIAN_POINT('Origin',(0.,-0.995,0.));
#50259=CARTESIAN_POINT('',(-0.24505,-0.995,-3.00099698131059E-17));
#62870=UNCERTAINTY_MEASURE_WITH_UNIT(LENGTH_MEASURE(0.001),#62985,
'DISTANCE_ACCURACY_VALUE',
'Maximum model space distance between geometric entities at asserted c
onnectivities');
#62885=UNCERTAINTY_MEASURE_WITH_UNIT(LENGTH_MEASURE(0.001),#62985,
'DISTANCE_ACCURACY_VALUE',
'Maximum model space distance between geometric entities at asserted c
onnectivities');
#62969=(
GEOMETRIC_REPRESENTATION_CONTEXT(3)
GLOBAL_UNCERTAINTY_ASSIGNED_CONTEXT((#62870))
GLOBAL_UNIT_ASSIGNED_CONTEXT((#62985,#62987,#62988))
REPRESENTATION_CONTEXT('','3D')
);
#62984=(
GEOMETRIC_REPRESENTATION_CONTEXT(3)
GLOBAL_UNCERTAINTY_ASSIGNED_CONTEXT((#62885))
GLOBAL_UNIT_ASSIGNED_CONTEXT((#62985,#62987,#62988))
REPRESENTATION_CONTEXT('','3D')
);
#62985=(
LENGTH_UNIT()
NAMED_UNIT(*)
SI_UNIT(.CENTI.,.METRE.)
);
#62987=(
NAMED_UNIT(*)
PLANE_ANGLE_UNIT()
SI_UNIT($,.RADIAN.)
);
#62988=(
NAMED_UNIT(*)
SI_UNIT($,.STERADIAN.)
SOLID_ANGLE_UNIT()
);
#63072=SHAPE_DEFINITION_REPRESENTATION(#63263,#63432);
#63263=PRODUCT_DEFINITION_SHAPE('',$,#63531);
#63432=SHAPE_REPRESENTATION('',(#25981),#62969);
#63447=PRODUCT_DEFINITION_CONTEXT('part definition',#63743,'design');
#63531=PRODUCT_DEFINITION('M5x30 frame screw (1)','M5x30 frame screw (1)',
#63629,#63447);
#63629=PRODUCT_DEFINITION_FORMATION('',$,#63828);
#63743=APPLICATION_CONTEXT(
'Core Data for Automotive Mechanical Design Process');
#63744=PRODUCT_CONTEXT('part definition',#63743,'mechanical');
#63828=PRODUCT('M5x30 frame screw (1)','M5x30 frame screw (1)',
'M5x30 frame screw (1)',(#63744));
#63913=COLOUR_RGB('Black',0.12,0.14,0.17);
#63914=FILL_AREA_STYLE_COLOUR('',#63913);
#63915=FILL_AREA_STYLE('',(#63914));
#63916=SURFACE_STYLE_FILL_AREA(#63915);
#63917=SURFACE_SIDE_STYLE('',(#63916));
#63918=SURFACE_STYLE_USAGE(.BOTH.,#63917);
#63919=PRESENTATION_STYLE_ASSIGNMENT((#63918));
ENDSEC;
END-ISO-10303-21;
